ISO-10303-21;
HEADER;
/* Generated by software containing ST-Developer
 * from STEP Tools, Inc. (www.steptools.com) 
 */

FILE_DESCRIPTION(
/* description */ ('PAT-026'),
/* implementation_level */ '2;1');

FILE_NAME(
/* name */ 'Socket Set Screw - M5x8.step',
/* time_stamp */ '2026-10-28T22:25:58-07:00',
/* author */ (''),
/* organization */ (''),
/* preprocessor_version */ 'ST-DEVELOPER v20.2',
/* originating_system */ 'Autodesk Translation Framework v15.17.0.0',
/* authorisation */ '');

FILE_SCHEMA (('AUTOMOTIVE_DESIGN { 1 0 10303 214 3 1 1 }'));
ENDSEC;

DATA;
#10=MECHANICAL_DESIGN_GEOMETRIC_PRESENTATION_REPRESENTATION('',(#151),#12343);
#113=CONICAL_SURFACE('',#8019,0.235,0.785398163397448);
#114=CONICAL_SURFACE('',#8023,0.2125,0.785398163397448);
#129=SHAPE_REPRESENTATION_RELATIONSHIP('SRR','None',#12407,#140);
#140=ADVANCED_BREP_SHAPE_REPRESENTATION('',(#160),#12342);
#151=STYLED_ITEM('',(#12540),#160);
#160=MANIFOLD_SOLID_BREP('Body1',#7359);
#193=FACE_BOUND('',#1387,.T.);
#544=PLANE('',#8010);
#545=PLANE('',#8011);
#546=PLANE('',#8012);
#547=PLANE('',#8013);
#548=PLANE('',#8014);
#549=PLANE('',#8015);
#550=PLANE('',#8016);
#551=PLANE('',#8017);
#552=PLANE('',#8025);
#944=FACE_OUTER_BOUND('',#1379,.T.);
#945=FACE_OUTER_BOUND('',#1380,.T.);
#946=FACE_OUTER_BOUND('',#1381,.T.);
#947=FACE_OUTER_BOUND('',#1382,.T.);
#948=FACE_OUTER_BOUND('',#1383,.T.);
#949=FACE_OUTER_BOUND('',#1384,.T.);
#950=FACE_OUTER_BOUND('',#1385,.T.);
#951=FACE_OUTER_BOUND('',#1386,.T.);
#952=FACE_OUTER_BOUND('',#1388,.T.);
#953=FACE_OUTER_BOUND('',#1389,.T.);
#954=FACE_OUTER_BOUND('',#1390,.T.);
#955=FACE_OUTER_BOUND('',#1391,.T.);
#1379=EDGE_LOOP('',(#6861,#6862,#6863,#6864));
#1380=EDGE_LOOP('',(#6865,#6866,#6867,#6868));
#1381=EDGE_LOOP('',(#6869,#6870,#6871,#6872));
#1382=EDGE_LOOP('',(#6873,#6874,#6875,#6876));
#1383=EDGE_LOOP('',(#6877,#6878,#6879,#6880));
#1384=EDGE_LOOP('',(#6881,#6882,#6883,#6884));
#1385=EDGE_LOOP('',(#6885,#6886,#6887,#6888,#6889,#6890));
#1386=EDGE_LOOP('',(#6891));
#1387=EDGE_LOOP('',(#6892,#6893,#6894,#6895,#6896,#6897));
#1388=EDGE_LOOP('',(#6898,#6899,#6900,#6901));
#1389=EDGE_LOOP('',(#6902,#6903,#6904,#6905));
#1390=EDGE_LOOP('',(#6906,#6907,#6908,#6909));
#1391=EDGE_LOOP('',(#6910));
#2243=LINE('',#12248,#3115);
#2244=LINE('',#12250,#3116);
#2245=LINE('',#12252,#3117);
#2246=LINE('',#12253,#3118);
#2247=LINE('',#12256,#3119);
#2248=LINE('',#12258,#3120);
#2249=LINE('',#12259,#3121);
#2250=LINE('',#12262,#3122);
#2251=LINE('',#12264,#3123);
#2252=LINE('',#12265,#3124);
#2253=LINE('',#12268,#3125);
#2254=LINE('',#12270,#3126);
#2255=LINE('',#12271,#3127);
#2256=LINE('',#12274,#3128);
#2257=LINE('',#12276,#3129);
#2258=LINE('',#12277,#3130);
#2259=LINE('',#12279,#3131);
#2260=LINE('',#12280,#3132);
#2261=LINE('',#12288,#3133);
#2262=LINE('',#12292,#3134);
#2263=LINE('',#12296,#3135);
#3115=VECTOR('',#9953,1.);
#3116=VECTOR('',#9954,1.);
#3117=VECTOR('',#9955,1.);
#3118=VECTOR('',#9956,1.);
#3119=VECTOR('',#9959,1.);
#3120=VECTOR('',#9960,1.);
#3121=VECTOR('',#9961,1.);
#3122=VECTOR('',#9964,1.);
#3123=VECTOR('',#9965,1.);
#3124=VECTOR('',#9966,1.);
#3125=VECTOR('',#9969,1.);
#3126=VECTOR('',#9970,1.);
#3127=VECTOR('',#9971,1.);
#3128=VECTOR('',#9974,1.);
#3129=VECTOR('',#9975,1.);
#3130=VECTOR('',#9976,1.);
#3131=VECTOR('',#9979,1.);
#3132=VECTOR('',#9980,1.);
#3133=VECTOR('',#9991,0.235);
#3134=VECTOR('',#9996,0.25);
#3135=VECTOR('',#10001,0.2125);
#3257=CIRCLE('',#8018,0.22);
#3258=CIRCLE('',#8020,0.24505);
#3259=CIRCLE('',#8022,0.24505);
#3260=CIRCLE('',#8024,0.175);
#3877=VERTEX_POINT('',#12246);
#3878=VERTEX_POINT('',#12247);
#3879=VERTEX_POINT('',#12249);
#3880=VERTEX_POINT('',#12251);
#3881=VERTEX_POINT('',#12255);
#3882=VERTEX_POINT('',#12257);
#3883=VERTEX_POINT('',#12261);
#3884=VERTEX_POINT('',#12263);
#3885=VERTEX_POINT('',#12267);
#3886=VERTEX_POINT('',#12269);
#3887=VERTEX_POINT('',#12273);
#3888=VERTEX_POINT('',#12275);
#3889=VERTEX_POINT('',#12283);
#3890=VERTEX_POINT('',#12286);
#3891=VERTEX_POINT('',#12290);
#3892=VERTEX_POINT('',#12294);
#4874=EDGE_CURVE('',#3877,#3878,#2243,.T.);
#4875=EDGE_CURVE('',#3877,#3879,#2244,.T.);
#4876=EDGE_CURVE('',#3879,#3880,#2245,.T.);
#4877=EDGE_CURVE('',#3878,#3880,#2246,.T.);
#4878=EDGE_CURVE('',#3881,#3877,#2247,.T.);
#4879=EDGE_CURVE('',#3881,#3882,#2248,.T.);
#4880=EDGE_CURVE('',#3882,#3879,#2249,.T.);
#4881=EDGE_CURVE('',#3883,#3881,#2250,.T.);
#4882=EDGE_CURVE('',#3883,#3884,#2251,.T.);
#4883=EDGE_CURVE('',#3884,#3882,#2252,.T.);
#4884=EDGE_CURVE('',#3885,#3883,#2253,.T.);
#4885=EDGE_CURVE('',#3885,#3886,#2254,.T.);
#4886=EDGE_CURVE('',#3886,#3884,#2255,.T.);
#4887=EDGE_CURVE('',#3887,#3885,#2256,.T.);
#4888=EDGE_CURVE('',#3887,#3888,#2257,.T.);
#4889=EDGE_CURVE('',#3888,#3886,#2258,.T.);
#4890=EDGE_CURVE('',#3878,#3887,#2259,.T.);
#4891=EDGE_CURVE('',#3880,#3888,#2260,.T.);
#4892=EDGE_CURVE('',#3889,#3889,#3257,.T.);
#4893=EDGE_CURVE('',#3890,#3890,#3258,.T.);
#4894=EDGE_CURVE('',#3890,#3889,#2261,.T.);
#4895=EDGE_CURVE('',#3891,#3891,#3259,.F.);
#4896=EDGE_CURVE('',#3891,#3890,#2262,.T.);
#4897=EDGE_CURVE('',#3892,#3892,#3260,.T.);
#4898=EDGE_CURVE('',#3892,#3891,#2263,.T.);
#6861=ORIENTED_EDGE('',*,*,#4874,.F.);
#6862=ORIENTED_EDGE('',*,*,#4875,.T.);
#6863=ORIENTED_EDGE('',*,*,#4876,.T.);
#6864=ORIENTED_EDGE('',*,*,#4877,.F.);
#6865=ORIENTED_EDGE('',*,*,#4878,.F.);
#6866=ORIENTED_EDGE('',*,*,#4879,.T.);
#6867=ORIENTED_EDGE('',*,*,#4880,.T.);
#6868=ORIENTED_EDGE('',*,*,#4875,.F.);
#6869=ORIENTED_EDGE('',*,*,#4881,.F.);
#6870=ORIENTED_EDGE('',*,*,#4882,.T.);
#6871=ORIENTED_EDGE('',*,*,#4883,.T.);
#6872=ORIENTED_EDGE('',*,*,#4879,.F.);
#6873=ORIENTED_EDGE('',*,*,#4884,.F.);
#6874=ORIENTED_EDGE('',*,*,#4885,.T.);
#6875=ORIENTED_EDGE('',*,*,#4886,.T.);
#6876=ORIENTED_EDGE('',*,*,#4882,.F.);
#6877=ORIENTED_EDGE('',*,*,#4887,.F.);
#6878=ORIENTED_EDGE('',*,*,#4888,.T.);
#6879=ORIENTED_EDGE('',*,*,#4889,.T.);
#6880=ORIENTED_EDGE('',*,*,#4885,.F.);
#6881=ORIENTED_EDGE('',*,*,#4890,.F.);
#6882=ORIENTED_EDGE('',*,*,#4877,.T.);
#6883=ORIENTED_EDGE('',*,*,#4891,.T.);
#6884=ORIENTED_EDGE('',*,*,#4888,.F.);
#6885=ORIENTED_EDGE('',*,*,#4891,.F.);
#6886=ORIENTED_EDGE('',*,*,#4876,.F.);
#6887=ORIENTED_EDGE('',*,*,#4880,.F.);
#6888=ORIENTED_EDGE('',*,*,#4883,.F.);
#6889=ORIENTED_EDGE('',*,*,#4886,.F.);
#6890=ORIENTED_EDGE('',*,*,#4889,.F.);
#6891=ORIENTED_EDGE('',*,*,#4892,.F.);
#6892=ORIENTED_EDGE('',*,*,#4874,.T.);
#6893=ORIENTED_EDGE('',*,*,#4890,.T.);
#6894=ORIENTED_EDGE('',*,*,#4887,.T.);
#6895=ORIENTED_EDGE('',*,*,#4884,.T.);
#6896=ORIENTED_EDGE('',*,*,#4881,.T.);
#6897=ORIENTED_EDGE('',*,*,#4878,.T.);
#6898=ORIENTED_EDGE('',*,*,#4893,.F.);
#6899=ORIENTED_EDGE('',*,*,#4894,.T.);
#6900=ORIENTED_EDGE('',*,*,#4892,.T.);
#6901=ORIENTED_EDGE('',*,*,#4894,.F.);
#6902=ORIENTED_EDGE('',*,*,#4895,.F.);
#6903=ORIENTED_EDGE('',*,*,#4896,.T.);
#6904=ORIENTED_EDGE('',*,*,#4893,.T.);
#6905=ORIENTED_EDGE('',*,*,#4896,.F.);
#6906=ORIENTED_EDGE('',*,*,#4897,.F.);
#6907=ORIENTED_EDGE('',*,*,#4898,.T.);
#6908=ORIENTED_EDGE('',*,*,#4895,.T.);
#6909=ORIENTED_EDGE('',*,*,#4898,.F.);
#6910=ORIENTED_EDGE('',*,*,#4897,.T.);
#6943=CYLINDRICAL_SURFACE('',#8021,0.24505);
#7335=ADVANCED_FACE('',(#944),#544,.F.);
#7336=ADVANCED_FACE('',(#945),#545,.F.);
#7337=ADVANCED_FACE('',(#946),#546,.F.);
#7338=ADVANCED_FACE('',(#947),#547,.F.);
#7339=ADVANCED_FACE('',(#948),#548,.F.);
#7340=ADVANCED_FACE('',(#949),#549,.F.);
#7341=ADVANCED_FACE('',(#950),#550,.F.);
#7342=ADVANCED_FACE('',(#951,#193),#551,.T.);
#7343=ADVANCED_FACE('',(#952),#113,.T.);
#7344=ADVANCED_FACE('',(#953),#6943,.T.);
#7345=ADVANCED_FACE('',(#954),#114,.T.);
#7346=ADVANCED_FACE('',(#955),#552,.T.);
#7359=CLOSED_SHELL('',(#7335,#7336,#7337,#7338,#7339,#7340,#7341,#7342,
#7343,#7344,#7345,#7346));
#8009=AXIS2_PLACEMENT_3D('',#12244,#9949,#9950);
#8010=AXIS2_PLACEMENT_3D('',#12245,#9951,#9952);
#8011=AXIS2_PLACEMENT_3D('',#12254,#9957,#9958);
#8012=AXIS2_PLACEMENT_3D('',#12260,#9962,#9963);
#8013=AXIS2_PLACEMENT_3D('',#12266,#9967,#9968);
#8014=AXIS2_PLACEMENT_3D('',#12272,#9972,#9973);
#8015=AXIS2_PLACEMENT_3D('',#12278,#9977,#9978);
#8016=AXIS2_PLACEMENT_3D('',#12281,#9981,#9982);
#8017=AXIS2_PLACEMENT_3D('',#12282,#9983,#9984);
#8018=AXIS2_PLACEMENT_3D('',#12284,#9985,#9986);
#8019=AXIS2_PLACEMENT_3D('',#12285,#9987,#9988);
#8020=AXIS2_PLACEMENT_3D('',#12287,#9989,#9990);
#8021=AXIS2_PLACEMENT_3D('',#12289,#9992,#9993);
#8022=AXIS2_PLACEMENT_3D('',#12291,#9994,#9995);
#8023=AXIS2_PLACEMENT_3D('',#12293,#9997,#9998);
#8024=AXIS2_PLACEMENT_3D('',#12295,#9999,#10000);
#8025=AXIS2_PLACEMENT_3D('',#12297,#10002,#10003);
#9949=DIRECTION('axis',(0.,0.,1.));
#9950=DIRECTION('refdir',(1.,0.,0.));
#9951=DIRECTION('center_axis',(0.866025403784439,0.,-0.5));
#9952=DIRECTION('ref_axis',(0.5,0.,0.866025403784439));
#9953=DIRECTION('',(0.5,0.,0.866025403784439));
#9954=DIRECTION('',(0.,-1.,0.));
#9955=DIRECTION('',(0.5,0.,0.866025403784439));
#9956=DIRECTION('',(0.,-1.,0.));
#9957=DIRECTION('center_axis',(1.92296268638356E-16,0.,-1.));
#9958=DIRECTION('ref_axis',(1.,0.,1.92296268638356E-16));
#9959=DIRECTION('',(1.,0.,1.92296268638356E-16));
#9960=DIRECTION('',(0.,-1.,0.));
#9961=DIRECTION('',(1.,0.,1.92296268638356E-16));
#9962=DIRECTION('center_axis',(-0.866025403784439,0.,-0.5));
#9963=DIRECTION('ref_axis',(0.5,0.,-0.866025403784439));
#9964=DIRECTION('',(0.5,0.,-0.866025403784439));
#9965=DIRECTION('',(0.,-1.,0.));
#9966=DIRECTION('',(0.5,0.,-0.866025403784438));
#9967=DIRECTION('center_axis',(-0.866025403784439,0.,0.5));
#9968=DIRECTION('ref_axis',(-0.5,0.,-0.866025403784439));
#9969=DIRECTION('',(-0.5,0.,-0.866025403784439));
#9970=DIRECTION('',(0.,-1.,0.));
#9971=DIRECTION('',(-0.5,0.,-0.866025403784439));
#9972=DIRECTION('center_axis',(-1.92296268638356E-16,0.,1.));
#9973=DIRECTION('ref_axis',(-1.,0.,-1.92296268638356E-16));
#9974=DIRECTION('',(-1.,0.,-1.92296268638356E-16));
#9975=DIRECTION('',(0.,-1.,0.));
#9976=DIRECTION('',(-1.,0.,-1.92296268638356E-16));
#9977=DIRECTION('center_axis',(0.866025403784439,0.,0.5));
#9978=DIRECTION('ref_axis',(-0.5,0.,0.866025403784439));
#9979=DIRECTION('',(-0.5,0.,0.866025403784439));
#9980=DIRECTION('',(-0.5,0.,0.866025403784439));
#9981=DIRECTION('center_axis',(0.,-1.,0.));
#9982=DIRECTION('ref_axis',(0.,0.,-1.));
#9983=DIRECTION('center_axis',(0.,1.,0.));
#9984=DIRECTION('ref_axis',(0.,0.,1.));
#9985=DIRECTION('center_axis',(0.,-1.,0.));
#9986=DIRECTION('ref_axis',(1.,0.,0.));
#9987=DIRECTION('center_axis',(0.,-1.,0.));
#9988=DIRECTION('ref_axis',(1.,0.,0.));
#9989=DIRECTION('center_axis',(0.,-1.,0.));
#9990=DIRECTION('ref_axis',(1.,0.,0.));
#9991=DIRECTION('',(0.707106781186547,0.707106781186548,8.65956056235493E-17));
#9992=DIRECTION('center_axis',(0.,-1.,0.));
#9993=DIRECTION('ref_axis',(1.,0.,0.));
#9994=DIRECTION('center_axis',(0.,1.,0.));
#9995=DIRECTION('ref_axis',(1.,0.,0.));
#9996=DIRECTION('',(0.,1.,0.));
#9997=DIRECTION('center_axis',(0.,1.,0.));
#9998=DIRECTION('ref_axis',(1.,0.,0.));
#9999=DIRECTION('center_axis',(0.,-1.,0.));
#10000=DIRECTION('ref_axis',(1.,0.,0.));
#10001=DIRECTION('',(-0.707106781186547,0.707106781186548,-8.65956056235493E-17));
#10002=DIRECTION('center_axis',(0.,-1.,0.));
#10003=DIRECTION('ref_axis',(0.,0.,-1.));
#12244=CARTESIAN_POINT('',(0.,0.,0.));
#12245=CARTESIAN_POINT('Origin',(0.0721687836487032,0.,-0.125));
#12246=CARTESIAN_POINT('',(0.0721687836487032,0.,-0.125));
#12247=CARTESIAN_POINT('',(0.144337567297406,0.,0.));
#12248=CARTESIAN_POINT('',(0.117710979560879,0.,-0.0461186027918559));
#12249=CARTESIAN_POINT('',(0.0721687836487032,-0.25,-0.125));
#12250=CARTESIAN_POINT('',(0.0721687836487032,0.,-0.125));
#12251=CARTESIAN_POINT('',(0.144337567297406,-0.25,0.));
#12252=CARTESIAN_POINT('',(0.144337567297406,-0.25,0.));
#12253=CARTESIAN_POINT('',(0.144337567297406,0.,0.));
#12254=CARTESIAN_POINT('Origin',(-0.0721687836487032,0.,-0.125));
#12255=CARTESIAN_POINT('',(-0.0721687836487032,0.,-0.125));
#12256=CARTESIAN_POINT('',(0.0739156081756484,0.,-0.125));
#12257=CARTESIAN_POINT('',(-0.0721687836487032,-0.25,-0.125));
#12258=CARTESIAN_POINT('',(-0.0721687836487032,0.,-0.125));
#12259=CARTESIAN_POINT('',(0.0721687836487032,-0.25,-0.125));
#12260=CARTESIAN_POINT('Origin',(-0.144337567297406,0.,-4.16333634234434E-17));
#12261=CARTESIAN_POINT('',(-0.144337567297406,0.,-1.76762539787485E-17));
#12262=CARTESIAN_POINT('',(-0.0987953713852306,0.,-0.0788813972081442));
#12263=CARTESIAN_POINT('',(-0.144337567297406,-0.25,-2.77555756156289E-17));
#12264=CARTESIAN_POINT('',(-0.144337567297406,0.,-1.76762539787485E-17));
#12265=CARTESIAN_POINT('',(-0.0721687836487032,-0.25,-0.125));
#12266=CARTESIAN_POINT('Origin',(-0.0721687836487033,0.,0.125));
#12267=CARTESIAN_POINT('',(-0.0721687836487033,0.,0.125));
#12268=CARTESIAN_POINT('',(-0.0627109795608791,0.,0.141381397208144));
#12269=CARTESIAN_POINT('',(-0.0721687836487033,-0.25,0.125));
#12270=CARTESIAN_POINT('',(-0.0721687836487033,0.,0.125));
#12271=CARTESIAN_POINT('',(-0.144337567297406,-0.25,-1.76762539787485E-17));
#12272=CARTESIAN_POINT('Origin',(0.0721687836487032,0.,0.125));
#12273=CARTESIAN_POINT('',(0.0721687836487032,0.,0.125));
#12274=CARTESIAN_POINT('',(0.146084391824352,0.,0.125));
#12275=CARTESIAN_POINT('',(0.0721687836487032,-0.25,0.125));
#12276=CARTESIAN_POINT('',(0.0721687836487032,0.,0.125));
#12277=CARTESIAN_POINT('',(-0.0721687836487033,-0.25,0.125));
#12278=CARTESIAN_POINT('Origin',(0.144337567297406,0.,0.));
#12279=CARTESIAN_POINT('',(0.153795371385231,0.,-0.0163813972081441));
#12280=CARTESIAN_POINT('',(0.0721687836487032,-0.25,0.125));
#12281=CARTESIAN_POINT('Origin',(0.,-0.25,0.));
#12282=CARTESIAN_POINT('Origin',(0.22,0.,0.));
#12283=CARTESIAN_POINT('',(-0.22,-8.67361737988404E-18,-2.69422295812418E-17));
#12284=CARTESIAN_POINT('Origin',(0.,0.,0.));
#12285=CARTESIAN_POINT('Origin',(0.,-0.015,0.));
#12286=CARTESIAN_POINT('',(-0.24505,-0.02505,-3.00099698131059E-17));
#12287=CARTESIAN_POINT('Origin',(0.,-0.02505,0.));
#12288=CARTESIAN_POINT('',(-0.235,-0.015,-2.87791997799628E-17));
#12289=CARTESIAN_POINT('Origin',(0.,-0.3775,0.));
#12290=CARTESIAN_POINT('',(-0.24505,-0.72995,3.00099698131059E-17));
#12291=CARTESIAN_POINT('Origin',(0.,-0.72995,0.));
#12292=CARTESIAN_POINT('',(-0.24505,-0.3775,-3.00099698131059E-17));
#12293=CARTESIAN_POINT('Origin',(0.,-0.7625,0.));
#12294=CARTESIAN_POINT('',(-0.175,-0.8,-2.14313189850787E-17));
#12295=CARTESIAN_POINT('Origin',(0.,-0.8,0.));
#12296=CARTESIAN_POINT('',(-0.2125,-0.7625,-2.60237444818813E-17));
#12297=CARTESIAN_POINT('Origin',(0.,-0.8,0.));
#12328=UNCERTAINTY_MEASURE_WITH_UNIT(LENGTH_MEASURE(0.001),#12344,
'DISTANCE_ACCURACY_VALUE',
'Maximum model space distance between geometric entities at asserted c
onnectivities');
#12329=UNCERTAINTY_MEASURE_WITH_UNIT(LENGTH_MEASURE(0.001),#12344,
'DISTANCE_ACCURACY_VALUE',
'Maximum model space distance between geometric entities at asserted c
onnectivities');
#12342=(
GEOMETRIC_REPRESENTATION_CONTEXT(3)
GLOBAL_UNCERTAINTY_ASSIGNED_CONTEXT((#12328))
GLOBAL_UNIT_ASSIGNED_CONTEXT((#12344,#12346,#12347))
REPRESENTATION_CONTEXT('','3D')
);
#12343=(
GEOMETRIC_REPRESENTATION_CONTEXT(3)
GLOBAL_UNCERTAINTY_ASSIGNED_CONTEXT((#12329))
GLOBAL_UNIT_ASSIGNED_CONTEXT((#12344,#12346,#12347))
REPRESENTATION_CONTEXT('','3D')
);
#12344=(
LENGTH_UNIT()
NAMED_UNIT(*)
SI_UNIT(.CENTI.,.METRE.)
);
#12346=(
NAMED_UNIT(*)
PLANE_ANGLE_UNIT()
SI_UNIT($,.RADIAN.)
);
#12347=(
NAMED_UNIT(*)
SI_UNIT($,.STERADIAN.)
SOLID_ANGLE_UNIT()
);
#12360=SHAPE_DEFINITION_REPRESENTATION(#12376,#12407);
#12376=PRODUCT_DEFINITION_SHAPE('',$,#12421);
#12407=SHAPE_REPRESENTATION('',(#8009),#12342);
#12408=PRODUCT_DEFINITION_CONTEXT('part definition',#12449,'design');
#12421=PRODUCT_DEFINITION('Socket Set Screw - M5x8',
'Socket Set Screw - M5x8',#12434,#12408);
#12434=PRODUCT_DEFINITION_FORMATION('',$,#12463);
#12449=APPLICATION_CONTEXT(
'Core Data for Automotive Mechanical Design Process');
#12450=PRODUCT_CONTEXT('part definition',#12449,'mechanical');
#12463=PRODUCT('Socket Set Screw - M5x8','Socket Set Screw - M5x8',
'Socket Set Screw - M5x8',(#12450));
#12534=COLOUR_RGB('Black',0.12,0.14,0.17);
#12535=FILL_AREA_STYLE_COLOUR('',#12534);
#12536=FILL_AREA_STYLE('',(#12535));
#12537=SURFACE_STYLE_FILL_AREA(#12536);
#12538=SURFACE_SIDE_STYLE('',(#12537));
#12539=SURFACE_STYLE_USAGE(.BOTH.,#12538);
#12540=PRESENTATION_STYLE_ASSIGNMENT((#12539));
ENDSEC;
END-ISO-10303-21;
